ISO-10303-21;
HEADER;
/* Generated by software containing ST-Developer
 * from STEP Tools, Inc. (www.steptools.com) 
 */

FILE_DESCRIPTION(
/* description */ ('Independent vertical20-tooth ratchet advance with repeated integral-c
ounterweight gravity pawls, swinging drive lever, bronze sleeves and f
ully retained axle stacks.18degpertooth. Native revolutes; geometric c
ycle checking rather than automatic contact/rolling dynamics. Gravity 
closing checked from actual pawl center of mass. Backplate/foot suppor
ts unit. Fits, torque, holding force, wear and life unassigned.'),
/* implementation_level */ '2;1');

FILE_NAME(
/* name */ 'Main thrust washer.step',
/* time_stamp */ '2026-11-09T06:25:53-08:00',
/* author */ (''),
/* organization */ (''),
/* preprocessor_version */ 'ST-DEVELOPER v20.2',
/* originating_system */ 'Autodesk Translation Framework v15.17.0.0',
/* authorisation */ '');

FILE_SCHEMA (('AUTOMOTIVE_DESIGN { 1 0 10303 214 3 1 1 }'));
ENDSEC;

DATA;
#10=MECHANICAL_DESIGN_GEOMETRIC_PRESENTATION_REPRESENTATION('',(#133),#4643);
#105=SHAPE_REPRESENTATION_RELATIONSHIP('SRR','None',#4710,#119);
#119=ADVANCED_BREP_SHAPE_REPRESENTATION('',(#147),#4639);
#133=STYLED_ITEM('',(#4786),#147);
#147=MANIFOLD_SOLID_BREP('Body1',#2669);
#186=FACE_BOUND('',#622,.T.);
#187=FACE_BOUND('',#624,.T.);
#294=PLANE('',#3035);
#295=PLANE('',#3036);
#435=FACE_OUTER_BOUND('',#619,.T.);
#436=FACE_OUTER_BOUND('',#620,.T.);
#437=FACE_OUTER_BOUND('',#621,.T.);
#438=FACE_OUTER_BOUND('',#623,.T.);
#619=EDGE_LOOP('',(#2413,#2414,#2415,#2416));
#620=EDGE_LOOP('',(#2417,#2418,#2419,#2420));
#621=EDGE_LOOP('',(#2421));
#622=EDGE_LOOP('',(#2422));
#623=EDGE_LOOP('',(#2423));
#624=EDGE_LOOP('',(#2424));
#891=LINE('',#4524,#1153);
#892=LINE('',#4530,#1154);
#1153=VECTOR('',#3741,5.);
#1154=VECTOR('',#3748,10.);
#1225=CIRCLE('',#3030,5.);
#1226=CIRCLE('',#3031,5.);
#1227=CIRCLE('',#3033,10.);
#1228=CIRCLE('',#3034,10.);
#1445=VERTEX_POINT('',#4521);
#1446=VERTEX_POINT('',#4523);
#1447=VERTEX_POINT('',#4527);
#1448=VERTEX_POINT('',#4529);
#1771=EDGE_CURVE('',#1445,#1445,#1225,.T.);
#1772=EDGE_CURVE('',#1445,#1446,#891,.T.);
#1773=EDGE_CURVE('',#1446,#1446,#1226,.T.);
#1774=EDGE_CURVE('',#1447,#1447,#1227,.T.);
#1775=EDGE_CURVE('',#1447,#1448,#892,.T.);
#1776=EDGE_CURVE('',#1448,#1448,#1228,.T.);
#2413=ORIENTED_EDGE('',*,*,#1771,.F.);
#2414=ORIENTED_EDGE('',*,*,#1772,.T.);
#2415=ORIENTED_EDGE('',*,*,#1773,.T.);
#2416=ORIENTED_EDGE('',*,*,#1772,.F.);
#2417=ORIENTED_EDGE('',*,*,#1774,.F.);
#2418=ORIENTED_EDGE('',*,*,#1775,.T.);
#2419=ORIENTED_EDGE('',*,*,#1776,.T.);
#2420=ORIENTED_EDGE('',*,*,#1775,.F.);
#2421=ORIENTED_EDGE('',*,*,#1774,.T.);
#2422=ORIENTED_EDGE('',*,*,#1771,.T.);
#2423=ORIENTED_EDGE('',*,*,#1776,.F.);
#2424=ORIENTED_EDGE('',*,*,#1773,.F.);
#2502=CYLINDRICAL_SURFACE('',#3029,5.);
#2503=CYLINDRICAL_SURFACE('',#3032,10.);
#2641=ADVANCED_FACE('',(#435),#2502,.F.);
#2642=ADVANCED_FACE('',(#436),#2503,.T.);
#2643=ADVANCED_FACE('',(#437,#186),#294,.T.);
#2644=ADVANCED_FACE('',(#438,#187),#295,.F.);
#2669=CLOSED_SHELL('',(#2641,#2642,#2643,#2644));
#3028=AXIS2_PLACEMENT_3D('',#4519,#3735,#3736);
#3029=AXIS2_PLACEMENT_3D('',#4520,#3737,#3738);
#3030=AXIS2_PLACEMENT_3D('',#4522,#3739,#3740);
#3031=AXIS2_PLACEMENT_3D('',#4525,#3742,#3743);
#3032=AXIS2_PLACEMENT_3D('',#4526,#3744,#3745);
#3033=AXIS2_PLACEMENT_3D('',#4528,#3746,#3747);
#3034=AXIS2_PLACEMENT_3D('',#4531,#3749,#3750);
#3035=AXIS2_PLACEMENT_3D('',#4532,#3751,#3752);
#3036=AXIS2_PLACEMENT_3D('',#4533,#3753,#3754);
#3735=DIRECTION('axis',(0.,0.,1.));
#3736=DIRECTION('refdir',(1.,0.,0.));
#3737=DIRECTION('center_axis',(0.,0.,1.));
#3738=DIRECTION('ref_axis',(1.,0.,0.));
#3739=DIRECTION('center_axis',(0.,0.,-1.));
#3740=DIRECTION('ref_axis',(1.,0.,0.));
#3741=DIRECTION('',(0.,0.,-1.));
#3742=DIRECTION('center_axis',(0.,0.,-1.));
#3743=DIRECTION('ref_axis',(1.,0.,0.));
#3744=DIRECTION('center_axis',(0.,0.,1.));
#3745=DIRECTION('ref_axis',(1.,0.,0.));
#3746=DIRECTION('center_axis',(0.,0.,1.));
#3747=DIRECTION('ref_axis',(1.,0.,0.));
#3748=DIRECTION('',(0.,0.,-1.));
#3749=DIRECTION('center_axis',(0.,0.,1.));
#3750=DIRECTION('ref_axis',(1.,0.,0.));
#3751=DIRECTION('center_axis',(0.,0.,1.));
#3752=DIRECTION('ref_axis',(1.,0.,0.));
#3753=DIRECTION('center_axis',(0.,0.,1.));
#3754=DIRECTION('ref_axis',(1.,0.,0.));
#4519=CARTESIAN_POINT('',(0.,0.,0.));
#4520=CARTESIAN_POINT('Origin',(0.,0.,0.));
#4521=CARTESIAN_POINT('',(-5.,-6.12323399573677E-16,2.));
#4522=CARTESIAN_POINT('Origin',(0.,0.,2.));
#4523=CARTESIAN_POINT('',(-5.,-6.12323399573677E-16,0.));
#4524=CARTESIAN_POINT('',(-5.,-6.12323399573677E-16,0.));
#4525=CARTESIAN_POINT('Origin',(0.,0.,0.));
#4526=CARTESIAN_POINT('Origin',(0.,0.,0.));
#4527=CARTESIAN_POINT('',(-10.,-1.22464679914735E-15,2.));
#4528=CARTESIAN_POINT('Origin',(0.,0.,2.));
#4529=CARTESIAN_POINT('',(-10.,-1.22464679914735E-15,0.));
#4530=CARTESIAN_POINT('',(-10.,-1.22464679914735E-15,0.));
#4531=CARTESIAN_POINT('Origin',(0.,0.,0.));
#4532=CARTESIAN_POINT('Origin',(0.,0.,2.));
#4533=CARTESIAN_POINT('Origin',(0.,0.,0.));
#4623=UNCERTAINTY_MEASURE_WITH_UNIT(LENGTH_MEASURE(0.01),#4644,
'DISTANCE_ACCURACY_VALUE',
'Maximum model space distance between geometric entities at asserted c
onnectivities');
#4627=UNCERTAINTY_MEASURE_WITH_UNIT(LENGTH_MEASURE(0.01),#4644,
'DISTANCE_ACCURACY_VALUE',
'Maximum model space distance between geometric entities at asserted c
onnectivities');
#4639=(
GEOMETRIC_REPRESENTATION_CONTEXT(3)
GLOBAL_UNCERTAINTY_ASSIGNED_CONTEXT((#4623))
GLOBAL_UNIT_ASSIGNED_CONTEXT((#4644,#4646,#4647))
REPRESENTATION_CONTEXT('','3D')
);
#4643=(
GEOMETRIC_REPRESENTATION_CONTEXT(3)
GLOBAL_UNCERTAINTY_ASSIGNED_CONTEXT((#4627))
GLOBAL_UNIT_ASSIGNED_CONTEXT((#4644,#4646,#4647))
REPRESENTATION_CONTEXT('','3D')
);
#4644=(
LENGTH_UNIT()
NAMED_UNIT(*)
SI_UNIT(.MILLI.,.METRE.)
);
#4646=(
NAMED_UNIT(*)
PLANE_ANGLE_UNIT()
SI_UNIT($,.RADIAN.)
);
#4647=(
NAMED_UNIT(*)
SI_UNIT($,.STERADIAN.)
SOLID_ANGLE_UNIT()
);
#4659=SHAPE_DEFINITION_REPRESENTATION(#4674,#4710);
#4674=PRODUCT_DEFINITION_SHAPE('',$,#4726);
#4710=SHAPE_REPRESENTATION('',(#3028),#4639);
#4714=PRODUCT_DEFINITION_CONTEXT('part definition',#4761,'design');
#4726=PRODUCT_DEFINITION('Main thrust washer','Main thrust washer',#4741,
#4714);
#4741=PRODUCT_DEFINITION_FORMATION('',$,#4774);
#4761=APPLICATION_CONTEXT(
'Core Data for Automotive Mechanical Design Process');
#4762=PRODUCT_CONTEXT('part definition',#4761,'mechanical');
#4774=PRODUCT('Main thrust washer','Main thrust washer',$,(#4762));
#4786=PRESENTATION_STYLE_ASSIGNMENT((#4795));
#4795=SURFACE_STYLE_USAGE(.BOTH.,#4804);
#4804=SURFACE_SIDE_STYLE('',(#4813));
#4813=SURFACE_STYLE_FILL_AREA(#4822);
#4822=FILL_AREA_STYLE('Light gray',(#4831));
#4831=FILL_AREA_STYLE_COLOUR('Light gray',#4840);
#4840=COLOUR_RGB('Light gray',0.725490196078431,0.752941176470588,0.792156862745098);
ENDSEC;
END-ISO-10303-21;
